ISO-10303-21;
HEADER;
FILE_DESCRIPTION (('STEP AP214'),
    '1' );
FILE_NAME ('socket button head screw_iso_ISO 7380 - M4 x 8 - 8N.step',
    '2026-10-24T08:20:21',
    ( '' ),
    ( '' ),
    'SwSTEP 2.0',
    'SolidWorks 2026',
    '' );
FILE_SCHEMA (( 'AUTOMOTIVE_DESIGN' ));
ENDSEC;

DATA;
#7=PLANE ( 'NONE',  #3620 ) ;
#11=ORIENTED_EDGE ( 'NONE', *, *, #3486, .F. ) ;
#13=ORIENTED_EDGE ( 'NONE', *, *, #231, .T. ) ;
#14=CARTESIAN_POINT ( 'NONE',  ( 1.820000000000000062, 0.000000000000000000, 0.000000000000000000 ) ) ;
#18=VECTOR ( 'NONE', #3561, 1000.000000000000114 ) ;
#21=EDGE_LOOP ( 'NONE', ( #2313, #294, #1297, #1026, #1998 ) ) ;
#37=FACE_OUTER_BOUND ( 'NONE', #2030, .T. ) ;
#38=CARTESIAN_POINT ( 'NONE',  ( 0.000000000000000000, -0.7216878364870318308, -1.250000000000000000 ) ) ;
#43=PLANE ( 'NONE',  #1656 ) ;
#48=CARTESIAN_POINT ( 'NONE',  ( 1.300000000000000044, 0.000000000000000000, 0.000000000000000000 ) ) ;
#51=FACE_OUTER_BOUND ( 'NONE', #2108, .T. ) ;
#53=CARTESIAN_POINT ( 'NONE',  ( 2.021687836487040535, 0.000000000000000000, 2.168404344971008868E-16 ) ) ;
#55=DIRECTION ( 'NONE',  ( 1.000000000000000000, 0.000000000000000000, 0.000000000000000000 ) ) ;
#56=DIRECTION ( 'NONE',  ( -1.000000000000000000, 0.000000000000000000, -0.000000000000000000 ) ) ;
#65=EDGE_LOOP ( 'NONE', ( #2892, #2887, #2094, #2492 ) ) ;
#75=VECTOR ( 'NONE', #2409, 1000.000000000000114 ) ;
#76=FACE_OUTER_BOUND ( 'NONE', #2053, .T. ) ;
#79=VECTOR ( 'NONE', #1201, 1000.000000000000000 ) ;
#80=VERTEX_POINT ( 'NONE', #800 ) ;
#82=ORIENTED_EDGE ( 'NONE', *, *, #2472, .F. ) ;
#93=AXIS2_PLACEMENT_3D ( 'NONE', #3300, #56, #338 ) ;
#102=VERTEX_POINT ( 'NONE', #209 ) ;
#105=DIRECTION ( 'NONE',  ( -1.000000000000000000, 0.000000000000000000, 0.000000000000000000 ) ) ;
#108=ORIENTED_EDGE ( 'NONE', *, *, #561, .F. ) ;
#114=( NAMED_UNIT ( * ) SI_UNIT ( $, .STERADIAN. ) SOLID_ANGLE_UNIT ( ) );
#117=CARTESIAN_POINT ( 'NONE',  ( 1.820000000000000062, 3.799999999999999378, 0.000000000000000000 ) ) ;
#118=ORIENTED_EDGE ( 'NONE', *, *, #270, .T. ) ;
#122=CARTESIAN_POINT ( 'NONE',  ( 9.809999999999998721, 0.000000000000000000, 0.000000000000000000 ) ) ;
#125=SURFACE_STYLE_USAGE ( .BOTH. , #2878 ) ;
#129=CARTESIAN_POINT ( 'NONE',  ( 1.300000000000000044, 0.7216878364870328300, -1.250000000000000000 ) ) ;
#136=CARTESIAN_POINT ( 'NONE',  ( 1.300000000000000044, -1.082531754730548412, -0.6249999999999997780 ) ) ;
#149=FACE_OUTER_BOUND ( 'NONE', #2973, .T. ) ;
#156=CARTESIAN_POINT ( 'NONE',  ( 9.809999999999998721, 2.449293598294705921E-16, -1.999999999999999556 ) ) ;
#170=CARTESIAN_POINT ( 'NONE',  ( 10.20000000000000107, 0.000000000000000000, 1.610000000000000098 ) ) ;
#171=ORIENTED_EDGE ( 'NONE', *, *, #2472, .T. ) ;
#173=DIRECTION ( 'NONE',  ( 0.000000000000000000, 0.000000000000000000, 1.000000000000000000 ) ) ;
#175=DIRECTION ( 'NONE',  ( -0.000000000000000000, -0.4999999999999999445, -0.8660254037844387076 ) ) ;
#188=PLANE ( 'NONE',  #436 ) ;
#191=EDGE_CURVE ( 'NONE', #3559, #2247, #1971, .T. ) ;
#193=CONICAL_SURFACE ( 'NONE', #3677, 1732.050807568856271, 1.047197551196592524 ) ;
#197=CIRCLE ( 'NONE', #701, 0.2000000000000000944 ) ;
#204=AXIS2_PLACEMENT_3D ( 'NONE', #554, #3183, #2954 ) ;
#206=EDGE_CURVE ( 'NONE', #535, #3277, #1093, .T. ) ;
#209=CARTESIAN_POINT ( 'NONE',  ( 10.20000000000000107, 2.210487472460972205E-16, -1.610000000000000098 ) ) ;
#221=AXIS2_PLACEMENT_3D ( 'NONE', #1149, #559, #3521 ) ;
#231=EDGE_CURVE ( 'NONE', #2038, #698, #2551, .T. ) ;
#237=ADVANCED_FACE ( 'NONE', ( #1844, #3552 ), #2668, .F. ) ;
#241=CARTESIAN_POINT ( 'NONE',  ( 4.336808689942017736E-16, -0.7216878364870318308, 1.249999999999999778 ) ) ;
#249=ORIENTED_EDGE ( 'NONE', *, *, #1970, .F. ) ;
#253=DIRECTION ( 'NONE',  ( -1.000000000000000000, -0.000000000000000000, -0.000000000000000000 ) ) ;
#259=CIRCLE ( 'NONE', #954, 3.799999999999999378 ) ;
#262=DIRECTION ( 'NONE',  ( 0.000000000000000000, 0.000000000000000000, 1.000000000000000000 ) ) ;
#265=CARTESIAN_POINT ( 'NONE',  ( 1.300000000000000044, -1.082531754730548412, 0.6249999999999998890 ) ) ;
#266=TOROIDAL_SURFACE ( 'NONE', #3014, 2.199999999999999289, 0.2000000000000000111 ) ;
#267=FACE_OUTER_BOUND ( 'NONE', #1466, .T. ) ;
#270=EDGE_CURVE ( 'NONE', #1478, #2858, #2967, .T. ) ;
#271=LINE ( 'NONE', #3543, #2440 ) ;
#278=ADVANCED_FACE ( 'NONE', ( #3617 ), #2093, .F. ) ;
#279=VECTOR ( 'NONE', #1163, 1000.000000000000000 ) ;
#293=EDGE_LOOP ( 'NONE', ( #2519, #1807, #3422, #686 ) ) ;
#294=ORIENTED_EDGE ( 'NONE', *, *, #561, .T. ) ;
#295=ORIENTED_EDGE ( 'NONE', *, *, #2901, .F. ) ;
#298=CARTESIAN_POINT ( 'NONE',  ( 1.300000000000000044, 0.7216878364870328300, -1.250000000000000000 ) ) ;
#303=FACE_OUTER_BOUND ( 'NONE', #3792, .T. ) ;
#309=EDGE_LOOP ( 'NONE', ( #3770, #1309, #1724, #1607, #1596 ) ) ;
#312=ORIENTED_EDGE ( 'NONE', *, *, #486, .T. ) ;
#314=CARTESIAN_POINT ( 'NONE',  ( 10.20000000000000107, 0.000000000000000000, 0.000000000000000000 ) ) ;
#317=EDGE_CURVE ( 'NONE', #742, #102, #1576, .T. ) ;
#325=LINE ( 'NONE', #2051, #1264 ) ;
#337=LINE ( 'NONE', #298, #2756 ) ;
#338=DIRECTION ( 'NONE',  ( -0.000000000000000000, 0.000000000000000000, 1.000000000000000000 ) ) ;
#341=AXIS2_PLACEMENT_3D ( 'NONE', #470, #1696, #3451 ) ;
#347=EDGE_CURVE ( 'NONE', #818, #3065, #1184, .T. ) ;
#360=CARTESIAN_POINT ( 'NONE',  ( 1.300000000000000044, 0.7216878364870328300, -1.250000000000000000 ) ) ;
#386=VECTOR ( 'NONE', #1029, 1000.000000000000000 ) ;
#391=ORIENTED_EDGE ( 'NONE', *, *, #1172, .F. ) ;
#393=AXIS2_PLACEMENT_3D ( 'NONE', #1623, #717, #2482 ) ;
#398=CARTESIAN_POINT ( 'NONE',  ( 0.000000000000000000, -1.443375672974063884, -3.691112476943992763E-18 ) ) ;
#400=DIRECTION ( 'NONE',  ( -1.000000000000000000, -0.000000000000000000, -0.000000000000000000 ) ) ;
#408=ORIENTED_EDGE ( 'NONE', *, *, #2175, .T. ) ;
#410=LINE ( 'NONE', #2154, #523 ) ;
#413=LINE ( 'NONE', #3075, #777 ) ;
#417=EDGE_CURVE ( 'NONE', #3510, #535, #1487, .T. ) ;
#421=LINE ( 'NONE', #1326, #1502 ) ;
#428=LINE ( 'NONE', #2171, #969 ) ;
#433=ORIENTED_EDGE ( 'NONE', *, *, #2310, .F. ) ;
#436=AXIS2_PLACEMENT_3D ( 'NONE', #459, #1382, #173 ) ;
#442=AXIS2_PLACEMENT_3D ( 'NONE', #1630, #400, #2242 ) ;
#451=AXIS2_PLACEMENT_3D ( 'NONE', #1088, #2312, #3462 ) ;
#459=CARTESIAN_POINT ( 'NONE',  ( 1.300000000000000044, -0.7216878364870319418, 1.249999999999999778 ) ) ;
#465=VERTEX_POINT ( 'NONE', #3634 ) ;
#467=ADVANCED_FACE ( 'NONE', ( #1337 ), #1299, .T. ) ;
#470=CARTESIAN_POINT ( 'NONE',  ( 1.820000000000000062, 0.000000000000000000, 0.000000000000000000 ) ) ;
#473=ORIENTED_EDGE ( 'NONE', *, *, #3077, .F. ) ;
#476=CARTESIAN_POINT ( 'NONE',  ( 1.300000000000000044, 1.443375672974065216, 7.017607234860990640E-28 ) ) ;
#482=EDGE_CURVE ( 'NONE', #2228, #2253, #413, .T. ) ;
#483=ORIENTED_EDGE ( 'NONE', *, *, #3700, .T. ) ;
#486=EDGE_CURVE ( 'NONE', #1598, #2646, #2955, .T. ) ;
#488=CARTESIAN_POINT ( 'NONE',  ( 0.000000000000000000, 0.000000000000000000, 0.000000000000000000 ) ) ;
#489=ORIENTED_EDGE ( 'NONE', *, *, #2922, .F. ) ;
#491=ORIENTED_EDGE ( 'NONE', *, *, #1833, .T. ) ;
#500=FILL_AREA_STYLE_COLOUR ( '', #2522 ) ;
#508=MECHANICAL_DESIGN_GEOMETRIC_PRESENTATION_REPRESENTATION('',(#1945),#1017);
#512=LINE ( 'NONE', #1143, #279 ) ;
#513=VECTOR ( 'NONE', #2474, 1000.000000000000000 ) ;
#518=CIRCLE ( 'NONE', #3813, 4.324969328314201888 ) ;
#519=ORIENTED_EDGE ( 'NONE', *, *, #3486, .T. ) ;
#523=VECTOR ( 'NONE', #690, 1000.000000000000114 ) ;
#526=DIRECTION ( 'NONE',  ( 0.000000000000000000, 0.000000000000000000, 1.000000000000000000 ) ) ;
#535=VERTEX_POINT ( 'NONE', #2466 ) ;
#539=ORIENTED_EDGE ( 'NONE', *, *, #1536, .T. ) ;
#548=ORIENTED_EDGE ( 'NONE', *, *, #1378, .T. ) ;
#554=CARTESIAN_POINT ( 'NONE',  ( 2.200000000000000622, 0.000000000000000000, 0.000000000000000000 ) ) ;
#558=ORIENTED_EDGE ( 'NONE', *, *, #2721, .F. ) ;
#559=DIRECTION ( 'NONE',  ( -1.000000000000000000, -0.000000000000000000, -0.000000000000000000 ) ) ;
#561=EDGE_CURVE ( 'NONE', #2858, #2217, #1358, .T. ) ;
#565=DIRECTION ( 'NONE',  ( -1.000000000000000000, 0.000000000000000000, -0.000000000000000000 ) ) ;
#578=VECTOR ( 'NONE', #2424, 1000.000000000000000 ) ;
#584=AXIS2_PLACEMENT_3D ( 'NONE', #1486, #55, #3633 ) ;
#585=ORIENTED_EDGE ( 'NONE', *, *, #317, .T. ) ;
#591=CARTESIAN_POINT ( 'NONE',  ( 1.300000000000000044, 0.7216878364870328300, 1.249999999999999778 ) ) ;
#605=VERTEX_POINT ( 'NONE', #606 ) ;
#606=CARTESIAN_POINT ( 'NONE',  ( 2.200000000000000622, 0.000000000000000000, 2.199999999999999289 ) ) ;
#621=CARTESIAN_POINT ( 'NONE',  ( 1.300000000000000044, -0.7216878364870318308, -1.250000000000000000 ) ) ;
#628=ORIENTED_EDGE ( 'NONE', *, *, #206, .F. ) ;
#636=AXIS2_PLACEMENT_3D ( 'NONE', #1943, #2917, #1452 ) ;
#646=DIRECTION ( 'NONE',  ( -1.000000000000000000, -0.000000000000000000, -0.000000000000000000 ) ) ;
#647=DIRECTION ( 'NONE',  ( -1.000000000000000000, 0.000000000000000000, 0.000000000000000000 ) ) ;
#650=DIRECTION ( 'NONE',  ( 0.000000000000000000, 0.000000000000000000, 1.000000000000000000 ) ) ;
#654=MECHANICAL_DESIGN_GEOMETRIC_PRESENTATION_REPRESENTATION('',(#785),#2832);
#659=VECTOR ( 'NONE', #728, 1000.000000000000114 ) ;
#661=DIRECTION ( 'NONE',  ( -1.000000000000000000, -0.000000000000000000, -0.000000000000000000 ) ) ;
#672=FACE_OUTER_BOUND ( 'NONE', #3258, .T. ) ;
#679=PLANE ( 'NONE',  #2123 ) ;
#685=ADVANCED_FACE ( 'NONE', ( #1209 ), #2138, .T. ) ;
#686=ORIENTED_EDGE ( 'NONE', *, *, #2064, .F. ) ;
#688=VERTEX_POINT ( 'NONE', #265 ) ;
#690=DIRECTION ( 'NONE',  ( -0.000000000000000000, -0.5000000000000002220, 0.8660254037844384856 ) ) ;
#692=CARTESIAN_POINT ( 'NONE',  ( 1.300000000000000044, -0.7216878364870319418, 1.249999999999999778 ) ) ;
#698=VERTEX_POINT ( 'NONE', #1568 ) ;
#701=AXIS2_PLACEMENT_3D ( 'NONE', #3803, #2930, #772 ) ;
#705=DIRECTION ( 'NONE',  ( 0.000000000000000000, 1.224646799147353207E-16, -1.000000000000000000 ) ) ;
#708=VECTOR ( 'NONE', #3356, 999.9999999999998863 ) ;
#712=CIRCLE ( 'NONE', #1027, 1.899999999999999689 ) ;
#717=DIRECTION ( 'NONE',  ( 0.000000000000000000, 0.000000000000000000, -1.000000000000000000 ) ) ;
#718=CYLINDRICAL_SURFACE ( 'NONE', #1081, 3.799999999999999378 ) ;
#721=AXIS2_PLACEMENT_3D ( 'NONE', #122, #2532, #1880 ) ;
#727=EDGE_CURVE ( 'NONE', #80, #3822, #2957, .T. ) ;
#728=DIRECTION ( 'NONE',  ( -0.000000000000000000, -0.5000000000000002220, 0.8660254037844384856 ) ) ;
#730=ORIENTED_EDGE ( 'NONE', *, *, #2175, .F. ) ;
#737=CARTESIAN_POINT ( 'NONE',  ( 1.820000000000000062, 0.000000000000000000, 0.000000000000000000 ) ) ;
#742=VERTEX_POINT ( 'NONE', #3385 ) ;
#744=CARTESIAN_POINT ( 'NONE',  ( 1.820000000000000062, 0.000000000000000000, 3.799999999999999378 ) ) ;
#747=( LENGTH_UNIT ( ) NAMED_UNIT ( * ) SI_UNIT ( .MILLI., .METRE. ) );
#751=UNCERTAINTY_MEASURE_WITH_UNIT (LENGTH_MEASURE( 1.000000000000000082E-05 ), #1401, 'distance_accuracy_value', 'NONE');
#759=SPHERICAL_SURFACE ( 'NONE', #636, 4.324969328314201888 ) ;
#772=DIRECTION ( 'NONE',  ( 0.000000000000000000, -1.224646799147353207E-16, 1.000000000000000000 ) ) ;
#777=VECTOR ( 'NONE', #1283, 1000.000000000000000 ) ;
#785=STYLED_ITEM ( 'NONE', ( #3425 ), #1526 ) ;
#789=VECTOR ( 'NONE', #3057, 1000.000000000000114 ) ;
#790=ORIENTED_EDGE ( 'NONE', *, *, #2754, .F. ) ;
#794=PRODUCT_DEFINITION_CONTEXT ( 'detailed design', #1619, 'design' ) ;
#795=DIRECTION ( 'NONE',  ( -1.000000000000000000, -0.000000000000000000, -0.000000000000000000 ) ) ;
#799=ORIENTED_EDGE ( 'NONE', *, *, #2239, .T. ) ;
#800=CARTESIAN_POINT ( 'NONE',  ( 9.809999999999998721, 0.000000000000000000, 1.999999999999999556 ) ) ;
#817=( NAMED_UNIT ( * ) SI_UNIT ( $, .STERADIAN. ) SOLID_ANGLE_UNIT ( ) );
#818=VERTEX_POINT ( 'NONE', #398 ) ;
#820=CARTESIAN_POINT ( 'NONE',  ( 0.000000000000000000, 0.000000000000000000, 0.000000000000000000 ) ) ;
#824=ORIENTED_EDGE ( 'NONE', *, *, #482, .F. ) ;
#825=EDGE_CURVE ( 'NONE', #3629, #1478, #3262, .T. ) ;
#829=DIRECTION ( 'NONE',  ( -1.000000000000000000, -0.000000000000000000, -0.000000000000000000 ) ) ;
#867=EDGE_CURVE ( 'NONE', #2247, #1784, #1858, .T. ) ;
#880=DIRECTION ( 'NONE',  ( -1.000000000000000000, -0.000000000000000000, -0.000000000000000000 ) ) ;
#881=DIRECTION ( 'NONE',  ( -1.000000000000000000, -0.000000000000000000, -0.000000000000000000 ) ) ;
#892=EDGE_CURVE ( 'NONE', #102, #3822, #428, .T. ) ;
#901=ORIENTED_EDGE ( 'NONE', *, *, #191, .F. ) ;
#903=AXIS2_PLACEMENT_3D ( 'NONE', #3436, #1670, #2854 ) ;
#909=AXIS2_PLACEMENT_3D ( 'NONE', #692, #2213, #1874 ) ;
#934=CARTESIAN_POINT ( 'NONE',  ( 1.300000000000000044, 0.7216878364870328300, -1.250000000000000000 ) ) ;
#954=AXIS2_PLACEMENT_3D ( 'NONE', #14, #1256, #3035 ) ;
#955=ADVANCED_FACE ( 'NONE', ( #3098 ), #3714, .T. ) ;
#967=LINE ( 'NONE', #1786, #578 ) ;
#969=VECTOR ( 'NONE', #1622, 1000.000000000000000 ) ;
#981=ADVANCED_FACE ( 'NONE', ( #3358 ), #2481, .T. ) ;
#982=DIRECTION ( 'NONE',  ( 0.000000000000000000, 1.000000000000000000, 1.224646799147353207E-16 ) ) ;
#983=LINE ( 'NONE', #129, #513 ) ;
#984=EDGE_LOOP ( 'NONE', ( #539, #3539, #2270, #1291, #3298 ) ) ;
#986=EDGE_LOOP ( 'NONE', ( #433, #3523, #558, #473 ) ) ;
#989=CARTESIAN_POINT ( 'NONE',  ( 2.400000000000000799, 2.449293598294705428E-16, -1.999999999999999112 ) ) ;
#993=CARTESIAN_POINT ( 'NONE',  ( 0.000000000000000000, 0.000000000000000000, 0.000000000000000000 ) ) ;
#995=CARTESIAN_POINT ( 'NONE',  ( 1.300000000000000044, 0.000000000000000000, 0.000000000000000000 ) ) ;
#1000=EDGE_CURVE ( 'NONE', #1302, #2909, #1402, .T. ) ;
#1001=ORIENTED_EDGE ( 'NONE', *, *, #347, .T. ) ;
#1011=CARTESIAN_POINT ( 'NONE',  ( 0.000000000000000000, 0.7216878364870328300, 1.249999999999999778 ) ) ;
#1012=AXIS2_PLACEMENT_3D ( 'NONE', #360, #2430, #2449 ) ;
#1017=( GEOMETRIC_REPRESENTATION_CONTEXT ( 3 ) GLOBAL_UNCERTAINTY_ASSIGNED_CONTEXT ( ( #1372 ) ) GLOBAL_UNIT_ASSIGNED_CONTEXT ( ( #747, #1597, #114 ) ) REPRESENTATION_CONTEXT ( 'NONE', 'WORKASPACE' ) );
#1026=ORIENTED_EDGE ( 'NONE', *, *, #2239, .F. ) ;
#1027=AXIS2_PLACEMENT_3D ( 'NONE', #2233, #2526, #2775 ) ;
#1029=DIRECTION ( 'NONE',  ( -1.000000000000000000, -0.000000000000000000, -0.000000000000000000 ) ) ;
#1034=CARTESIAN_POINT ( 'NONE',  ( 1.300000000000000044, 0.000000000000000000, 0.000000000000000000 ) ) ;
#1041=VECTOR ( 'NONE', #3490, 1000.000000000000000 ) ;
#1044=CARTESIAN_POINT ( 'NONE',  ( 1.300000000000000044, -1.443375672974063884, -3.691112476943992763E-18 ) ) ;
#1061=PRODUCT_CONTEXT ( 'NONE', #3170, 'mechanical' ) ;
#1065=DIRECTION ( 'NONE',  ( 0.000000000000000000, 0.000000000000000000, 1.000000000000000000 ) ) ;
#1081=AXIS2_PLACEMENT_3D ( 'NONE', #993, #3115, #2549 ) ;
#1084=ORIENTED_EDGE ( 'NONE', *, *, #2901, .T. ) ;
#1085=CARTESIAN_POINT ( 'NONE',  ( 1.300000000000000044, -0.7216878364870318308, 1.249999999999999778 ) ) ;
#1088=CARTESIAN_POINT ( 'NONE',  ( 2.400000000000000799, 0.000000000000000000, 2.199999999999999289 ) ) ;
#1093=CIRCLE ( 'NONE', #221, 1.249999999999999778 ) ;
#1099=EDGE_CURVE ( 'NONE', #2038, #2858, #512, .T. ) ;
#1104=VECTOR ( 'NONE', #1788, 1000.000000000000000 ) ;
#1117=FACE_OUTER_BOUND ( 'NONE', #1586, .T. ) ;
#1122=FACE_OUTER_BOUND ( 'NONE', #21, .T. ) ;
#1131=FACE_OUTER_BOUND ( 'NONE', #65, .T. ) ;
#1134=TOROIDAL_SURFACE ( 'NONE', #1501, 2.199999999999999289, 0.2000000000000000111 ) ;
#1142=ORIENTED_EDGE ( 'NONE', *, *, #1099, .F. ) ;
#1143=CARTESIAN_POINT ( 'NONE',  ( 1.300000000000000044, 1.443375672974065216, 7.017607234860990640E-28 ) ) ;
#1146=CARTESIAN_POINT ( 'NONE',  ( 1.300000000000000044, 0.000000000000000000, 0.000000000000000000 ) ) ;
#1147=AXIS2_PLACEMENT_3D ( 'NONE', #3323, #3017, #3299 ) ;
#1149=CARTESIAN_POINT ( 'NONE',  ( 1.300000000000000044, 0.000000000000000000, 0.000000000000000000 ) ) ;
#1152=CYLINDRICAL_SURFACE ( 'NONE', #1814, 1.999999999999999112 ) ;
#1163=DIRECTION ( 'NONE',  ( -0.000000000000000000, 0.5000000000000001110, 0.8660254037844385966 ) ) ;
#1172=EDGE_CURVE ( 'NONE', #3629, #2659, #1396, .T. ) ;
#1177=CARTESIAN_POINT ( 'NONE',  ( 2.200000000000000622, 2.694222958124176020E-16, -2.199999999999999289 ) ) ;
#1184=LINE ( 'NONE', #38, #2889 ) ;
#1186=ADVANCED_FACE ( 'NONE', ( #76 ), #43, .T. ) ;
#1189=CARTESIAN_POINT ( 'NONE',  ( 1.300000000000000044, -0.7216878364870318308, -1.250000000000000000 ) ) ;
#1190=CARTESIAN_POINT ( 'NONE',  ( 1.820000000000000062, 0.000000000000000000, 0.000000000000000000 ) ) ;
#1193=ORIENTED_EDGE ( 'NONE', *, *, #1172, .T. ) ;
#1201=DIRECTION ( 'NONE',  ( -1.000000000000000000, -0.000000000000000000, -0.000000000000000000 ) ) ;
#1205=EDGE_CURVE ( 'NONE', #2381, #1598, #3826, .T. ) ;
#1209=FACE_OUTER_BOUND ( 'NONE', #984, .T. ) ;
#1210=VECTOR ( 'NONE', #3294, 1000.000000000000000 ) ;
#1211=DIRECTION ( 'NONE',  ( 0.000000000000000000, 0.000000000000000000, 1.000000000000000000 ) ) ;
#1214=VECTOR ( 'NONE', #3440, 1000.000000000000000 ) ;
#1215=DIRECTION ( 'NONE',  ( -0.000000000000000000, -0.5000000000000002220, 0.8660254037844384856 ) ) ;
#1216=ORIENTED_EDGE ( 'NONE', *, *, #1000, .T. ) ;
#1224=ORIENTED_EDGE ( 'NONE', *, *, #2216, .F. ) ;
#1237=PLANE ( 'NONE',  #3384 ) ;
#1240=ADVANCED_FACE ( 'NONE', ( #1864 ), #2455, .T. ) ;
#1243=DIRECTION ( 'NONE',  ( -0.000000000000000000, 0.4999999999999998890, -0.8660254037844387076 ) ) ;
#1251=EDGE_CURVE ( 'NONE', #3822, #2947, #3311, .T. ) ;
#1256=DIRECTION ( 'NONE',  ( -1.000000000000000000, -0.000000000000000000, -0.000000000000000000 ) ) ;
#1257=VECTOR ( 'NONE', #2323, 1000.000000000000114 ) ;
#1264=VECTOR ( 'NONE', #2692, 1000.000000000000000 ) ;
#1267=PLANE ( 'NONE',  #1012 ) ;
#1270=DIRECTION ( 'NONE',  ( 0.000000000000000000, 0.8660254037844387076, -0.4999999999999999445 ) ) ;
#1272=AXIS2_PLACEMENT_3D ( 'NONE', #2214, #3715, #1563 ) ;
#1280=CARTESIAN_POINT ( 'NONE',  ( 0.000000000000000000, -1.443375672974063884, -3.691112476943992763E-18 ) ) ;
#1283=DIRECTION ( 'NONE',  ( -0.000000000000000000, -1.000000000000000000, -0.000000000000000000 ) ) ;
#1291=ORIENTED_EDGE ( 'NONE', *, *, #347, .F. ) ;
#1297=ORIENTED_EDGE ( 'NONE', *, *, #2658, .T. ) ;
#1299=PLANE ( 'NONE',  #393 ) ;
#1300=DIRECTION ( 'NONE',  ( 0.000000000000000000, 0.000000000000000000, 1.000000000000000000 ) ) ;
#1302=VERTEX_POINT ( 'NONE', #744 ) ;
#1309=ORIENTED_EDGE ( 'NONE', *, *, #2920, .T. ) ;
#1326=CARTESIAN_POINT ( 'NONE',  ( 1.300000000000000044, -0.7216878364870318308, 1.249999999999999778 ) ) ;
#1337=FACE_OUTER_BOUND ( 'NONE', #2966, .T. ) ;
#1339=EDGE_CURVE ( 'NONE', #2659, #688, #2201, .T. ) ;
#1345=PRODUCT_DEFINITION_FORMATION_WITH_SPECIFIED_SOURCE ( 'ANY', '', #3397, .NOT_KNOWN. ) ;
#1348=EDGE_CURVE ( 'NONE', #2909, #1784, #1840, .T. ) ;
#1350=CYLINDRICAL_SURFACE ( 'NONE', #3261, 3.799999999999999378 ) ;
#1358=LINE ( 'NONE', #1649, #1214 ) ;
#1359=CARTESIAN_POINT ( 'NONE',  ( 9.809999999999998721, 0.000000000000000000, 0.000000000000000000 ) ) ;
#1364=( NAMED_UNIT ( * ) SI_UNIT ( $, .STERADIAN. ) SOLID_ANGLE_UNIT ( ) );
#1372=UNCERTAINTY_MEASURE_WITH_UNIT (LENGTH_MEASURE( 1.000000000000000082E-05 ), #747, 'distance_accuracy_value', 'NONE');
#1378=EDGE_CURVE ( 'NONE', #465, #2228, #3121, .T. ) ;
#1382=DIRECTION ( 'NONE',  ( -1.000000000000000000, 0.000000000000000000, 0.000000000000000000 ) ) ;
#1383=( LENGTH_UNIT ( ) NAMED_UNIT ( * ) SI_UNIT ( .MILLI., .METRE. ) );
#1391=FACE_OUTER_BOUND ( 'NONE', #309, .T. ) ;
#1392=VERTEX_POINT ( 'NONE', #3762 ) ;
#1396=LINE ( 'NONE', #3790, #1041 ) ;
#1401=( LENGTH_UNIT ( ) NAMED_UNIT ( * ) SI_UNIT ( .MILLI., .METRE. ) );
#1402=CIRCLE ( 'NONE', #1404, 3.799999999999999378 ) ;
#1404=AXIS2_PLACEMENT_3D ( 'NONE', #737, #3074, #2777 ) ;
#1409=ORIENTED_EDGE ( 'NONE', *, *, #2491, .T. ) ;
#1416=DIRECTION ( 'NONE',  ( -1.000000000000000000, -0.000000000000000000, -0.000000000000000000 ) ) ;
#1439=ORIENTED_EDGE ( 'NONE', *, *, #317, .F. ) ;
#1443=CARTESIAN_POINT ( 'NONE',  ( 1.300000000000000044, 0.000000000000000000, 0.000000000000000000 ) ) ;
#1452=DIRECTION ( 'NONE',  ( 0.000000000000000000, 1.000000000000000000, 0.000000000000000000 ) ) ;
#1456=CARTESIAN_POINT ( 'NONE',  ( -997.9783121635130101, 0.000000000000000000, 0.000000000000000000 ) ) ;
#1466=EDGE_LOOP ( 'NONE', ( #2807, #2915, #3512, #118, #3164 ) ) ;
#1476=CARTESIAN_POINT ( 'NONE',  ( 1.300000000000000044, 1.082531754730548856, 0.6250000000000006661 ) ) ;
#1478=VERTEX_POINT ( 'NONE', #1476 ) ;
#1482=ORIENTED_EDGE ( 'NONE', *, *, #2447, .F. ) ;
#1485=EDGE_LOOP ( 'NONE', ( #3595, #249, #1671, #2789 ) ) ;
#1486=CARTESIAN_POINT ( 'NONE',  ( 2.400000000000000799, 0.000000000000000000, 0.000000000000000000 ) ) ;
#1487=LINE ( 'NONE', #1588, #789 ) ;
#1492=DIRECTION ( 'NONE',  ( -1.000000000000000000, -0.000000000000000000, -0.000000000000000000 ) ) ;
#1494=LINE ( 'NONE', #591, #2943 ) ;
#1501=AXIS2_PLACEMENT_3D ( 'NONE', #3243, #881, #3227 ) ;
#1502=VECTOR ( 'NONE', #647, 1000.000000000000000 ) ;
#1509=CIRCLE ( 'NONE', #3756, 1.999999999999999112 ) ;
#1514=ADVANCED_FACE ( 'NONE', ( #3215 ), #7, .F. ) ;
#1515=DIRECTION ( 'NONE',  ( -1.000000000000000000, 0.000000000000000000, 0.000000000000000000 ) ) ;
#1519=ORIENTED_EDGE ( 'NONE', *, *, #206, .T. ) ;
#1524=CARTESIAN_POINT ( 'NONE',  ( 1.820000000000000062, -3.800000000000000266, -4.653657836759940757E-16 ) ) ;
#1526=ADVANCED_BREP_SHAPE_REPRESENTATION ( '', ( #3253, #2207 ), #2713 ) ;
#1530=DIRECTION ( 'NONE',  ( -1.000000000000000000, -0.000000000000000000, -0.000000000000000000 ) ) ;
#1536=EDGE_CURVE ( 'NONE', #1392, #3277, #3249, .T. ) ;
#1539=ADVANCED_FACE ( 'NONE', ( #1131 ), #1152, .T. ) ;
#1540=EDGE_CURVE ( 'NONE', #3277, #3156, #3504, .T. ) ;
#1541=CLOSED_SHELL ( 'NONE', ( #278, #1925, #2926, #1539, #3829, #955, #1733, #1863, #2069, #237, #2630, #1240, #1514, #2999, #1186, #685, #1669, #3042, #3370, #467, #3195, #981, #2731, #1806, #2222, #2555, #1582 ) ) ;
#1546=ORIENTED_EDGE ( 'NONE', *, *, #2251, .F. ) ;
#1563=DIRECTION ( 'NONE',  ( 0.000000000000000000, 0.000000000000000000, 1.000000000000000000 ) ) ;
#1568=CARTESIAN_POINT ( 'NONE',  ( 0.000000000000000000, 0.7216878364870328300, -1.250000000000000000 ) ) ;
#1569=DIRECTION ( 'NONE',  ( -1.000000000000000000, 0.000000000000000000, -0.000000000000000000 ) ) ;
#1576=CIRCLE ( 'NONE', #2459, 1.610000000000000098 ) ;
#1582=ADVANCED_FACE ( 'NONE', ( #267 ), #193, .F. ) ;
#1586=EDGE_LOOP ( 'NONE', ( #1592, #3789, #2611, #3671, #3173 ) ) ;
#1587=DIRECTION ( 'NONE',  ( 0.000000000000000000, 1.000000000000000000, 0.000000000000000000 ) ) ;
#1588=CARTESIAN_POINT ( 'NONE',  ( 2.021687836487040535, 2.655529440325959183E-32, -2.168404344971008868E-16 ) ) ;
#1589=PLANE ( 'NONE',  #3310 ) ;
#1592=ORIENTED_EDGE ( 'NONE', *, *, #191, .T. ) ;
#1596=ORIENTED_EDGE ( 'NONE', *, *, #2658, .F. ) ;
#1597=( NAMED_UNIT ( * ) PLANE_ANGLE_UNIT ( ) SI_UNIT ( $, .RADIAN. ) );
#1598=VERTEX_POINT ( 'NONE', #1861 ) ;
#1600=DIRECTION ( 'NONE',  ( -1.000000000000000000, -0.000000000000000000, -0.000000000000000000 ) ) ;
#1607=ORIENTED_EDGE ( 'NONE', *, *, #1378, .F. ) ;
#1618=DIRECTION ( 'NONE',  ( -1.000000000000000000, -0.000000000000000000, -0.000000000000000000 ) ) ;
#1619=APPLICATION_CONTEXT ( 'automotive_design' ) ;
#1622=DIRECTION ( 'NONE',  ( -0.7071067811865492381, 8.659560562354911904E-17, -0.7071067811865457964 ) ) ;
#1623=CARTESIAN_POINT ( 'NONE',  ( 1.300000000000000044, -0.7216878364870318308, 1.249999999999999778 ) ) ;
#1630=CARTESIAN_POINT ( 'NONE',  ( 2.200000000000000178, 0.000000000000000000, 0.000000000000000000 ) ) ;
#1631=AXIS2_PLACEMENT_3D ( 'NONE', #1190, #2090, #2363 ) ;
#1642=CYLINDRICAL_SURFACE ( 'NONE', #1950, 1.999999999999999112 ) ;
#1645=EDGE_LOOP ( 'NONE', ( #3280, #1980, #1519, #2562, #408 ) ) ;
#1649=CARTESIAN_POINT ( 'NONE',  ( 1.300000000000000044, 1.443375672974065216, 7.017607234860990640E-28 ) ) ;
#1656=AXIS2_PLACEMENT_3D ( 'NONE', #3626, #1270, #3659 ) ;
#1669=ADVANCED_FACE ( 'NONE', ( #2176 ), #1267, .T. ) ;
#1670=DIRECTION ( 'NONE',  ( 0.000000000000000000, -0.8660254037844385966, 0.5000000000000001110 ) ) ;
#1671=ORIENTED_EDGE ( 'NONE', *, *, #3077, .T. ) ;
#1679=CARTESIAN_POINT ( 'NONE',  ( 0.000000000000000000, 0.7216878364870328300, 1.249999999999999778 ) ) ;
#1683=ORIENTED_EDGE ( 'NONE', *, *, #3565, .F. ) ;
#1694=FILL_AREA_STYLE ('',( #500 ) ) ;
#1696=DIRECTION ( 'NONE',  ( -1.000000000000000000, -0.000000000000000000, -0.000000000000000000 ) ) ;
#1701=CIRCLE ( 'NONE', #2073, 1.249999999999999778 ) ;
#1705=PRODUCT_DEFINITION ( 'UNKNOWN', '', #1345, #794 ) ;
#1708=FACE_OUTER_BOUND ( 'NONE', #1485, .T. ) ;
#1709=ORIENTED_EDGE ( 'NONE', *, *, #1339, .T. ) ;
#1718=ORIENTED_EDGE ( 'NONE', *, *, #3186, .T. ) ;
#1723=ORIENTED_EDGE ( 'NONE', *, *, #3679, .T. ) ;
#1724=ORIENTED_EDGE ( 'NONE', *, *, #3514, .T. ) ;
#1733=ADVANCED_FACE ( 'NONE', ( #303, #1848 ), #679, .T. ) ;
#1748=DIRECTION ( 'NONE',  ( 0.000000000000000000, -0.4999999999999998890, 0.8660254037844387076 ) ) ;
#1753=CIRCLE ( 'NONE', #2192, 2.199999999999999289 ) ;
#1768=CARTESIAN_POINT ( 'NONE',  ( 1.300000000000000044, 1.082531754730548856, -0.6250000000000003331 ) ) ;
#1779=CARTESIAN_POINT ( 'NONE',  ( 2.200000000000000178, 0.000000000000000000, 3.799999999999999378 ) ) ;
#1784=VERTEX_POINT ( 'NONE', #3140 ) ;
#1786=CARTESIAN_POINT ( 'NONE',  ( 1.300000000000000044, -0.7216878364870318308, 1.249999999999999778 ) ) ;
#1788=DIRECTION ( 'NONE',  ( -1.000000000000000000, 0.000000000000000000, 0.000000000000000000 ) ) ;
#1792=CARTESIAN_POINT ( 'NONE',  ( 0.000000000000000000, 0.000000000000000000, 0.000000000000000000 ) ) ;
#1806=ADVANCED_FACE ( 'NONE', ( #2261 ), #188, .T. ) ;
#1807=ORIENTED_EDGE ( 'NONE', *, *, #3083, .T. ) ;
#1814=AXIS2_PLACEMENT_3D ( 'NONE', #1792, #2593, #2923 ) ;
#1817=CARTESIAN_POINT ( 'NONE',  ( 3.885274725274726393, -8.673617379884035472E-16, 0.000000000000000000 ) ) ;
#1828=VECTOR ( 'NONE', #2387, 999.9999999999998863 ) ;
#1829=UNCERTAINTY_MEASURE_WITH_UNIT (LENGTH_MEASURE( 1.000000000000000082E-05 ), #1383, 'distance_accuracy_value', 'NONE');
#1833=EDGE_CURVE ( 'NONE', #2247, #3559, #3372, .T. ) ;
#1840=CIRCLE ( 'NONE', #341, 3.799999999999999378 ) ;
#1843=CARTESIAN_POINT ( 'NONE',  ( 0.000000000000000000, 0.000000000000000000, 3.799999999999999378 ) ) ;
#1844=FACE_BOUND ( 'NONE', #3433, .T. ) ;
#1847=DIRECTION ( 'NONE',  ( 0.000000000000000000, 0.000000000000000000, 1.000000000000000000 ) ) ;
#1848=FACE_BOUND ( 'NONE', #3445, .T. ) ;
#1857=ORIENTED_EDGE ( 'NONE', *, *, #482, .T. ) ;
#1858=LINE ( 'NONE', #2528, #3702 ) ;
#1861=CARTESIAN_POINT ( 'NONE',  ( 8.673617379884035472E-16, -1.899999999999999689, -3.490243377569955075E-16 ) ) ;
#1863=ADVANCED_FACE ( 'NONE', ( #149 ), #759, .T. ) ;
#1864=FACE_OUTER_BOUND ( 'NONE', #293, .T. ) ;
#1874=DIRECTION ( 'NONE',  ( 0.000000000000000000, 0.000000000000000000, 1.000000000000000000 ) ) ;
#1877=DIRECTION ( 'NONE',  ( 0.000000000000000000, 0.000000000000000000, 1.000000000000000000 ) ) ;
#1880=DIRECTION ( 'NONE',  ( 0.000000000000000000, 0.000000000000000000, 1.000000000000000000 ) ) ;
#1890=ORIENTED_EDGE ( 'NONE', *, *, #2965, .T. ) ;
#1904=FACE_OUTER_BOUND ( 'NONE', #2436, .T. ) ;
#1915=DIRECTION ( 'NONE',  ( -1.000000000000000000, 0.000000000000000000, 0.000000000000000000 ) ) ;
#1921=DIRECTION ( 'NONE',  ( 0.000000000000000000, 0.000000000000000000, 1.000000000000000000 ) ) ;
#1925=ADVANCED_FACE ( 'NONE', ( #3189 ), #1134, .F. ) ;
#1930=ORIENTED_EDGE ( 'NONE', *, *, #1970, .T. ) ;
#1942=ORIENTED_EDGE ( 'NONE', *, *, #2920, .F. ) ;
#1943=CARTESIAN_POINT ( 'NONE',  ( 3.885274725274726393, -8.673617379884035472E-16, 0.000000000000000000 ) ) ;
#1945=STYLED_ITEM('',(#3881),#3253);
#1950=AXIS2_PLACEMENT_3D ( 'NONE', #3396, #1618, #1065 ) ;
#1957=LINE ( 'NONE', #476, #2077 ) ;
#1970=EDGE_CURVE ( 'NONE', #605, #3181, #1753, .T. ) ;
#1971=CIRCLE ( 'NONE', #2150, 3.799999999999999378 ) ;
#1980=ORIENTED_EDGE ( 'NONE', *, *, #417, .T. ) ;
#1998=ORIENTED_EDGE ( 'NONE', *, *, #231, .F. ) ;
#2001=VERTEX_POINT ( 'NONE', #2685 ) ;
#2011=VECTOR ( 'NONE', #3361, 1000.000000000000000 ) ;
#2016=ORIENTED_EDGE ( 'NONE', *, *, #3679, .F. ) ;
#2030=EDGE_LOOP ( 'NONE', ( #1142, #790, #2438 ) ) ;
#2031=VECTOR ( 'NONE', #175, 999.9999999999998863 ) ;
#2038=VERTEX_POINT ( 'NONE', #3618 ) ;
#2048=ORIENTED_EDGE ( 'NONE', *, *, #2747, .T. ) ;
#2051=CARTESIAN_POINT ( 'NONE',  ( 0.000000000000000000, 0.7216878364870328300, -1.250000000000000000 ) ) ;
#2053=EDGE_LOOP ( 'NONE', ( #1709, #1409, #1718, #295, #2907 ) ) ;
#2064=EDGE_CURVE ( 'NONE', #3822, #80, #2382, .T. ) ;
#2069=ADVANCED_FACE ( 'NONE', ( #1904 ), #718, .T. ) ;
#2073=AXIS2_PLACEMENT_3D ( 'NONE', #1146, #2617, #2315 ) ;
#2077=VECTOR ( 'NONE', #3749, 1000.000000000000000 ) ;
#2090=DIRECTION ( 'NONE',  ( -1.000000000000000000, -0.000000000000000000, -0.000000000000000000 ) ) ;
#2093=CONICAL_SURFACE ( 'NONE', #2203, 1732.050807568856271, 1.047197551196592524 ) ;
#2094=ORIENTED_EDGE ( 'NONE', *, *, #2787, .T. ) ;
#2100=DIRECTION ( 'NONE',  ( 0.000000000000000000, 0.000000000000000000, 1.000000000000000000 ) ) ;
#2103=EDGE_LOOP ( 'NONE', ( #2607, #391, #730 ) ) ;
#2108=EDGE_LOOP ( 'NONE', ( #1482, #1942, #3607 ) ) ;
#2110=CARTESIAN_POINT ( 'NONE',  ( 1.300000000000000044, -0.7216878364870318308, -1.250000000000000000 ) ) ;
#2117=DIRECTION ( 'NONE',  ( 0.000000000000000000, 0.000000000000000000, 1.000000000000000000 ) ) ;
#2123=AXIS2_PLACEMENT_3D ( 'NONE', #3587, #1569, #2763 ) ;
#2138=PLANE ( 'NONE',  #3084 ) ;
#2143=CARTESIAN_POINT ( 'NONE',  ( 10.20000000000000107, 0.000000000000000000, 0.000000000000000000 ) ) ;
#2150=AXIS2_PLACEMENT_3D ( 'NONE', #2859, #1416, #3211 ) ;
#2151=DIRECTION ( 'NONE',  ( 0.000000000000000000, 0.000000000000000000, 1.000000000000000000 ) ) ;
#2154=CARTESIAN_POINT ( 'NONE',  ( 1.300000000000000044, 0.7216878364870328300, 1.249999999999999778 ) ) ;
#2171=CARTESIAN_POINT ( 'NONE',  ( 10.20000000000000107, 1.971681346627238735E-16, -1.610000000000000098 ) ) ;
#2175=EDGE_CURVE ( 'NONE', #688, #3629, #3686, .T. ) ;
#2176=FACE_OUTER_BOUND ( 'NONE', #3034, .T. ) ;
#2179=DIRECTION ( 'NONE',  ( 0.000000000000000000, 0.000000000000000000, 1.000000000000000000 ) ) ;
#2189=DIRECTION ( 'NONE',  ( -1.000000000000000000, -0.000000000000000000, -0.000000000000000000 ) ) ;
#2192=AXIS2_PLACEMENT_3D ( 'NONE', #2319, #3040, #2117 ) ;
#2200=CIRCLE ( 'NONE', #2446, 1.249999999999999778 ) ;
#2201=LINE ( 'NONE', #1044, #2031 ) ;
#2203=AXIS2_PLACEMENT_3D ( 'NONE', #2393, #2427, #262 ) ;
#2207=AXIS2_PLACEMENT_3D ( 'NONE', #820, #2246, #3194 ) ;
#2213=DIRECTION ( 'NONE',  ( -1.000000000000000000, 0.000000000000000000, 0.000000000000000000 ) ) ;
#2214=CARTESIAN_POINT ( 'NONE',  ( 8.673617379884035472E-16, 0.000000000000000000, 0.000000000000000000 ) ) ;
#2216=EDGE_CURVE ( 'NONE', #742, #80, #2237, .T. ) ;
#2217=VERTEX_POINT ( 'NONE', #2849 ) ;
#2220=ORIENTED_EDGE ( 'NONE', *, *, #2310, .T. ) ;
#2222=ADVANCED_FACE ( 'NONE', ( #2467 ), #1589, .T. ) ;
#2228=VERTEX_POINT ( 'NONE', #1011 ) ;
#2233=CARTESIAN_POINT ( 'NONE',  ( 8.673617379884035472E-16, 0.000000000000000000, 0.000000000000000000 ) ) ;
#2237=LINE ( 'NONE', #170, #2011 ) ;
#2239=EDGE_CURVE ( 'NONE', #698, #465, #3755, .T. ) ;
#2242=DIRECTION ( 'NONE',  ( 0.000000000000000000, 0.000000000000000000, 1.000000000000000000 ) ) ;
#2243=SURFACE_STYLE_FILL_AREA ( #1694 ) ;
#2246=DIRECTION ( 'NONE',  ( 0.000000000000000000, 0.000000000000000000, 1.000000000000000000 ) ) ;
#2247=VERTEX_POINT ( 'NONE', #3533 ) ;
#2251=EDGE_CURVE ( 'NONE', #3277, #688, #1701, .T. ) ;
#2253=VERTEX_POINT ( 'NONE', #241 ) ;
#2259=ORIENTED_EDGE ( 'NONE', *, *, #2754, .T. ) ;
#2261=FACE_OUTER_BOUND ( 'NONE', #3247, .T. ) ;
#2269=AXIS2_PLACEMENT_3D ( 'NONE', #3054, #1600, #2497 ) ;
#2270=ORIENTED_EDGE ( 'NONE', *, *, #2521, .T. ) ;
#2281=AXIS2_PLACEMENT_3D ( 'NONE', #995, #661, #1847 ) ;
#2302=EDGE_LOOP ( 'NONE', ( #2864, #519, #3162, #489, #82 ) ) ;
#2305=DIRECTION ( 'NONE',  ( -0.000000000000000000, 0.000000000000000000, 1.000000000000000000 ) ) ;
#2310=EDGE_CURVE ( 'NONE', #3181, #605, #3008, .T. ) ;
#2312=DIRECTION ( 'NONE',  ( 0.000000000000000000, -1.000000000000000000, 0.000000000000000000 ) ) ;
#2313=ORIENTED_EDGE ( 'NONE', *, *, #1099, .T. ) ;
#2315=DIRECTION ( 'NONE',  ( 0.000000000000000000, 0.000000000000000000, 1.000000000000000000 ) ) ;
#2319=CARTESIAN_POINT ( 'NONE',  ( 2.200000000000000622, 0.000000000000000000, 0.000000000000000000 ) ) ;
#2323=DIRECTION ( 'NONE',  ( -0.000000000000000000, 0.4999999999999998890, -0.8660254037844387076 ) ) ;
#2341=AXIS2_PLACEMENT_3D ( 'NONE', #3335, #705, #982 ) ;
#2350=ORIENTED_EDGE ( 'NONE', *, *, #1833, .F. ) ;
#2358=EDGE_CURVE ( 'NONE', #2381, #1302, #259, .T. ) ;
#2360=ORIENTED_EDGE ( 'NONE', *, *, #2521, .F. ) ;
#2362=CARTESIAN_POINT ( 'NONE',  ( 10.20000000000000107, 0.000000000000000000, 0.000000000000000000 ) ) ;
#2363=DIRECTION ( 'NONE',  ( 0.000000000000000000, 0.000000000000000000, 1.000000000000000000 ) ) ;
#2381=VERTEX_POINT ( 'NONE', #1524 ) ;
#2382=CIRCLE ( 'NONE', #3070, 1.999999999999999556 ) ;
#2384=DIRECTION ( 'NONE',  ( -1.000000000000000000, 0.000000000000000000, 0.000000000000000000 ) ) ;
#2387=DIRECTION ( 'NONE',  ( -0.000000000000000000, -0.4999999999999999445, -0.8660254037844387076 ) ) ;
#2391=ORIENTED_EDGE ( 'NONE', *, *, #2491, .F. ) ;
#2392=CARTESIAN_POINT ( 'NONE',  ( 2.400000000000000799, 0.000000000000000000, 0.000000000000000000 ) ) ;
#2393=CARTESIAN_POINT ( 'NONE',  ( -997.9783121635130101, 0.000000000000000000, 0.000000000000000000 ) ) ;
#2396=AXIS2_PLACEMENT_3D ( 'NONE', #48, #1530, #3536 ) ;
#2406=ORIENTED_EDGE ( 'NONE', *, *, #867, .F. ) ;
#2409=DIRECTION ( 'NONE',  ( -0.5000000000000044409, 0.000000000000000000, 0.8660254037844360431 ) ) ;
#2410=ORIENTED_EDGE ( 'NONE', *, *, #892, .T. ) ;
#2424=DIRECTION ( 'NONE',  ( -0.000000000000000000, -1.000000000000000000, -0.000000000000000000 ) ) ;
#2426=PLANE ( 'NONE',  #1147 ) ;
#2427=DIRECTION ( 'NONE',  ( -1.000000000000000000, -0.000000000000000000, -0.000000000000000000 ) ) ;
#2430=DIRECTION ( 'NONE',  ( 0.000000000000000000, 0.000000000000000000, 1.000000000000000000 ) ) ;
#2434=EDGE_CURVE ( 'NONE', #3510, #3629, #3838, .T. ) ;
#2436=EDGE_LOOP ( 'NONE', ( #2406, #491, #2048, #3530, #11 ) ) ;
#2438=ORIENTED_EDGE ( 'NONE', *, *, #3006, .F. ) ;
#2440=VECTOR ( 'NONE', #1515, 1000.000000000000000 ) ;
#2446=AXIS2_PLACEMENT_3D ( 'NONE', #1443, #829, #3488 ) ;
#2447=EDGE_CURVE ( 'NONE', #3016, #3629, #967, .T. ) ;
#2449=DIRECTION ( 'NONE',  ( 1.000000000000000000, 0.000000000000000000, -0.000000000000000000 ) ) ;
#2455=CONICAL_SURFACE ( 'NONE', #3333, 1.610000000000000098, 0.7853981633974458365 ) ;
#2459=AXIS2_PLACEMENT_3D ( 'NONE', #314, #880, #2684 ) ;
#2460=DIRECTION ( 'NONE',  ( 0.000000000000000000, 0.000000000000000000, 1.000000000000000000 ) ) ;
#2466=CARTESIAN_POINT ( 'NONE',  ( 1.300000000000000044, 0.000000000000000000, -1.250000000000000000 ) ) ;
#2467=FACE_OUTER_BOUND ( 'NONE', #3546, .T. ) ;
#2472=EDGE_CURVE ( 'NONE', #2909, #2646, #518, .T. ) ;
#2474=DIRECTION ( 'NONE',  ( -0.000000000000000000, 1.000000000000000000, -0.000000000000000000 ) ) ;
#2481=PLANE ( 'NONE',  #909 ) ;
#2482=DIRECTION ( 'NONE',  ( -1.000000000000000000, 0.000000000000000000, -0.000000000000000000 ) ) ;
#2491=EDGE_CURVE ( 'NONE', #688, #1392, #3574, .T. ) ;
#2492=ORIENTED_EDGE ( 'NONE', *, *, #2965, .F. ) ;
#2497=DIRECTION ( 'NONE',  ( 0.000000000000000000, 0.000000000000000000, 1.000000000000000000 ) ) ;
#2519=ORIENTED_EDGE ( 'NONE', *, *, #892, .F. ) ;
#2520=PLANE ( 'NONE',  #3315 ) ;
#2521=EDGE_CURVE ( 'NONE', #3156, #3065, #2808, .T. ) ;
#2522=COLOUR_RGB ( '',1.000000000000000000, 0.9490196078431372140, 0.9098039215686274384 ) ;
#2526=DIRECTION ( 'NONE',  ( -1.000000000000000000, -0.000000000000000000, -0.000000000000000000 ) ) ;
#2528=CARTESIAN_POINT ( 'NONE',  ( 0.000000000000000000, 4.653657836759941744E-16, -3.799999999999999378 ) ) ;
#2532=DIRECTION ( 'NONE',  ( -1.000000000000000000, -0.000000000000000000, -0.000000000000000000 ) ) ;
#2535=( NAMED_UNIT ( * ) PLANE_ANGLE_UNIT ( ) SI_UNIT ( $, .RADIAN. ) );
#2541=DIRECTION ( 'NONE',  ( 0.000000000000000000, -0.8660254037844385966, -0.5000000000000003331 ) ) ;
#2543=CARTESIAN_POINT ( 'NONE',  ( 1.300000000000000044, -0.7216878364870319418, 1.249999999999999778 ) ) ;
#2549=DIRECTION ( 'NONE',  ( 0.000000000000000000, 0.000000000000000000, 1.000000000000000000 ) ) ;
#2551=LINE ( 'NONE', #934, #1104 ) ;
#2555=ADVANCED_FACE ( 'NONE', ( #3053 ), #2520, .T. ) ;
#2561=DIRECTION ( 'NONE',  ( 0.000000000000000000, 0.000000000000000000, 1.000000000000000000 ) ) ;
#2562=ORIENTED_EDGE ( 'NONE', *, *, #2251, .T. ) ;
#2582=AXIS2_PLACEMENT_3D ( 'NONE', #2759, #3652, #1587 ) ;
#2593=DIRECTION ( 'NONE',  ( -1.000000000000000000, -0.000000000000000000, -0.000000000000000000 ) ) ;
#2607=ORIENTED_EDGE ( 'NONE', *, *, #1339, .F. ) ;
#2610=DIRECTION ( 'NONE',  ( 0.000000000000000000, 0.5000000000000002220, -0.8660254037844384856 ) ) ;
#2611=ORIENTED_EDGE ( 'NONE', *, *, #1348, .F. ) ;
#2617=DIRECTION ( 'NONE',  ( -1.000000000000000000, -0.000000000000000000, -0.000000000000000000 ) ) ;
#2630=ADVANCED_FACE ( 'NONE', ( #3727 ), #1642, .T. ) ;
#2635=AXIS2_PLACEMENT_3D ( 'NONE', #3220, #795, #3168 ) ;
#2646=VERTEX_POINT ( 'NONE', #3458 ) ;
#2651=ORIENTED_EDGE ( 'NONE', *, *, #2721, .T. ) ;
#2658=EDGE_CURVE ( 'NONE', #2217, #465, #1957, .T. ) ;
#2659=VERTEX_POINT ( 'NONE', #1085 ) ;
#2660=CARTESIAN_POINT ( 'NONE',  ( 1.300000000000000044, -1.443375672974063884, -3.691112476943992763E-18 ) ) ;
#2668=PLANE ( 'NONE',  #93 ) ;
#2679=ORIENTED_EDGE ( 'NONE', *, *, #1205, .F. ) ;
#2681=CARTESIAN_POINT ( 'NONE',  ( 1.300000000000000044, -1.443375672974063884, -3.691112476943992763E-18 ) ) ;
#2684=DIRECTION ( 'NONE',  ( 0.000000000000000000, 0.000000000000000000, 1.000000000000000000 ) ) ;
#2685=CARTESIAN_POINT ( 'NONE',  ( 2.400000000000000799, 0.000000000000000000, 1.999999999999999112 ) ) ;
#2687=ORIENTED_EDGE ( 'NONE', *, *, #3514, .F. ) ;
#2692=DIRECTION ( 'NONE',  ( -0.000000000000000000, 1.000000000000000000, -0.000000000000000000 ) ) ;
#2713=( GEOMETRIC_REPRESENTATION_CONTEXT ( 3 ) GLOBAL_UNCERTAINTY_ASSIGNED_CONTEXT ( ( #1829 ) ) GLOBAL_UNIT_ASSIGNED_CONTEXT ( ( #1383, #2535, #1364 ) ) REPRESENTATION_CONTEXT ( 'NONE', 'WORKASPACE' ) );
#2721=EDGE_CURVE ( 'NONE', #2001, #2947, #3252, .T. ) ;
#2731=ADVANCED_FACE ( 'NONE', ( #37 ), #2426, .T. ) ;
#2740=EDGE_LOOP ( 'NONE', ( #901, #2350 ) ) ;
#2747=EDGE_CURVE ( 'NONE', #3559, #1302, #2994, .T. ) ;
#2749=ORIENTED_EDGE ( 'NONE', *, *, #727, .F. ) ;
#2754=EDGE_CURVE ( 'NONE', #535, #2038, #337, .T. ) ;
#2756=VECTOR ( 'NONE', #3580, 1000.000000000000000 ) ;
#2757=CARTESIAN_POINT ( 'NONE',  ( 0.000000000000000000, 0.000000000000000000, 1.999999999999999112 ) ) ;
#2759=CARTESIAN_POINT ( 'NONE',  ( 3.885274725274726393, -8.673617379884035472E-16, 0.000000000000000000 ) ) ;
#2763=DIRECTION ( 'NONE',  ( -0.000000000000000000, 0.000000000000000000, 1.000000000000000000 ) ) ;
#2775=DIRECTION ( 'NONE',  ( 0.000000000000000000, 0.000000000000000000, 1.000000000000000000 ) ) ;
#2777=DIRECTION ( 'NONE',  ( 0.000000000000000000, 0.000000000000000000, 1.000000000000000000 ) ) ;
#2779=CARTESIAN_POINT ( 'NONE',  ( 1.300000000000000044, -0.7216878364870319418, 1.249999999999999778 ) ) ;
#2787=EDGE_CURVE ( 'NONE', #2947, #2001, #1509, .T. ) ;
#2789=ORIENTED_EDGE ( 'NONE', *, *, #2787, .F. ) ;
#2790=CARTESIAN_POINT ( 'NONE',  ( 1.300000000000000044, -0.7216878364870318308, -1.250000000000000000 ) ) ;
#2791=LINE ( 'NONE', #2757, #386 ) ;
#2797=ORIENTED_EDGE ( 'NONE', *, *, #3083, .F. ) ;
#2803=PRODUCT_DEFINITION_SHAPE ( 'NONE', 'NONE',  #1705 ) ;
#2807=ORIENTED_EDGE ( 'NONE', *, *, #417, .F. ) ;
#2808=LINE ( 'NONE', #2790, #3137 ) ;
#2811=ORIENTED_EDGE ( 'NONE', *, *, #1536, .F. ) ;
#2828=ORIENTED_EDGE ( 'NONE', *, *, #270, .F. ) ;
#2832=( GEOMETRIC_REPRESENTATION_CONTEXT ( 3 ) GLOBAL_UNCERTAINTY_ASSIGNED_CONTEXT ( ( #751 ) ) GLOBAL_UNIT_ASSIGNED_CONTEXT ( ( #1401, #3408, #817 ) ) REPRESENTATION_CONTEXT ( 'NONE', 'WORKASPACE' ) );
#2849=CARTESIAN_POINT ( 'NONE',  ( 1.300000000000000044, 1.443375672974065216, 7.017607234860990640E-28 ) ) ;
#2854=DIRECTION ( 'NONE',  ( 0.000000000000000000, -0.5000000000000001110, -0.8660254037844385966 ) ) ;
#2858=VERTEX_POINT ( 'NONE', #1768 ) ;
#2859=CARTESIAN_POINT ( 'NONE',  ( 2.200000000000000178, 0.000000000000000000, 0.000000000000000000 ) ) ;
#2864=ORIENTED_EDGE ( 'NONE', *, *, #1348, .T. ) ;
#2878=SURFACE_SIDE_STYLE ('',( #2243 ) ) ;
#2887=ORIENTED_EDGE ( 'NONE', *, *, #1251, .T. ) ;
#2889=VECTOR ( 'NONE', #1243, 1000.000000000000114 ) ;
#2891=CARTESIAN_POINT ( 'NONE',  ( 2.400000000000000799, 0.000000000000000000, 0.000000000000000000 ) ) ;
#2892=ORIENTED_EDGE ( 'NONE', *, *, #727, .T. ) ;
#2901=EDGE_CURVE ( 'NONE', #2253, #818, #3665, .T. ) ;
#2907=ORIENTED_EDGE ( 'NONE', *, *, #3700, .F. ) ;
#2909=VERTEX_POINT ( 'NONE', #117 ) ;
#2915=ORIENTED_EDGE ( 'NONE', *, *, #2434, .T. ) ;
#2917=DIRECTION ( 'NONE',  ( 0.000000000000000000, 0.000000000000000000, -1.000000000000000000 ) ) ;
#2920=EDGE_CURVE ( 'NONE', #1478, #3016, #410, .T. ) ;
#2922=EDGE_CURVE ( 'NONE', #2646, #1598, #712, .T. ) ;
#2923=DIRECTION ( 'NONE',  ( 0.000000000000000000, 0.000000000000000000, 1.000000000000000000 ) ) ;
#2926=ADVANCED_FACE ( 'NONE', ( #672 ), #2948, .T. ) ;
#2930=DIRECTION ( 'NONE',  ( -0.000000000000000000, 1.000000000000000000, 1.224646799147353207E-16 ) ) ;
#2943=VECTOR ( 'NONE', #1215, 1000.000000000000114 ) ;
#2946=CARTESIAN_POINT ( 'NONE',  ( 2.021687836487040535, 2.168404344971008868E-16, 0.000000000000000000 ) ) ;
#2947=VERTEX_POINT ( 'NONE', #989 ) ;
#2948=CONICAL_SURFACE ( 'NONE', #2269, 1.610000000000000098, 0.7853981633974458365 ) ;
#2954=DIRECTION ( 'NONE',  ( 0.000000000000000000, 0.000000000000000000, 1.000000000000000000 ) ) ;
#2955=CIRCLE ( 'NONE', #1272, 1.899999999999999689 ) ;
#2957=CIRCLE ( 'NONE', #721, 1.999999999999999556 ) ;
#2965=EDGE_CURVE ( 'NONE', #80, #2001, #2791, .T. ) ;
#2966=EDGE_LOOP ( 'NONE', ( #3219, #1193, #483, #824, #2687 ) ) ;
#2967=CIRCLE ( 'NONE', #2396, 1.249999999999999778 ) ;
#2971=EDGE_LOOP ( 'NONE', ( #3005, #108, #2828 ) ) ;
#2973=EDGE_LOOP ( 'NONE', ( #2679, #3287, #1216, #171, #3011 ) ) ;
#2976=DIRECTION ( 'NONE',  ( 1.000000000000000000, 0.000000000000000000, 0.000000000000000000 ) ) ;
#2987=ORIENTED_EDGE ( 'NONE', *, *, #1540, .F. ) ;
#2994=LINE ( 'NONE', #1843, #79 ) ;
#2999=ADVANCED_FACE ( 'NONE', ( #1708 ), #266, .F. ) ;
#3005=ORIENTED_EDGE ( 'NONE', *, *, #3564, .F. ) ;
#3006=EDGE_CURVE ( 'NONE', #2858, #535, #2200, .T. ) ;
#3008=CIRCLE ( 'NONE', #204, 2.199999999999999289 ) ;
#3011=ORIENTED_EDGE ( 'NONE', *, *, #486, .F. ) ;
#3014=AXIS2_PLACEMENT_3D ( 'NONE', #2891, #253, #2561 ) ;
#3016=VERTEX_POINT ( 'NONE', #3152 ) ;
#3017=DIRECTION ( 'NONE',  ( -1.000000000000000000, 0.000000000000000000, 0.000000000000000000 ) ) ;
#3034=EDGE_LOOP ( 'NONE', ( #1723, #2259, #13, #1683, #2360 ) ) ;
#3035=DIRECTION ( 'NONE',  ( 0.000000000000000000, 0.000000000000000000, 1.000000000000000000 ) ) ;
#3040=DIRECTION ( 'NONE',  ( -1.000000000000000000, -0.000000000000000000, -0.000000000000000000 ) ) ;
#3042=ADVANCED_FACE ( 'NONE', ( #1122 ), #3731, .T. ) ;
#3045=EDGE_CURVE ( 'NONE', #3181, #2947, #197, .T. ) ;
#3046=CARTESIAN_POINT ( 'NONE',  ( 0.000000000000000000, 2.449293598294705428E-16, -1.999999999999999112 ) ) ;
#3053=FACE_OUTER_BOUND ( 'NONE', #2103, .T. ) ;
#3054=CARTESIAN_POINT ( 'NONE',  ( 10.20000000000000107, 0.000000000000000000, 0.000000000000000000 ) ) ;
#3057=DIRECTION ( 'NONE',  ( -0.5000000000000044409, 1.060575238724903587E-16, -0.8660254037844360431 ) ) ;
#3062=DIRECTION ( 'NONE',  ( -1.000000000000000000, -0.000000000000000000, -0.000000000000000000 ) ) ;
#3065=VERTEX_POINT ( 'NONE', #3788 ) ;
#3070=AXIS2_PLACEMENT_3D ( 'NONE', #1359, #3383, #1877 ) ;
#3074=DIRECTION ( 'NONE',  ( -1.000000000000000000, -0.000000000000000000, -0.000000000000000000 ) ) ;
#3075=CARTESIAN_POINT ( 'NONE',  ( 0.000000000000000000, -0.7216878364870318308, 1.249999999999999778 ) ) ;
#3077=EDGE_CURVE ( 'NONE', #605, #2001, #3570, .T. ) ;
#3083=EDGE_CURVE ( 'NONE', #102, #742, #3760, .T. ) ;
#3084=AXIS2_PLACEMENT_3D ( 'NONE', #621, #3330, #1748 ) ;
#3088=VECTOR ( 'NONE', #646, 1000.000000000000000 ) ;
#3098=FACE_OUTER_BOUND ( 'NONE', #2302, .T. ) ;
#3115=DIRECTION ( 'NONE',  ( -1.000000000000000000, -0.000000000000000000, -0.000000000000000000 ) ) ;
#3121=LINE ( 'NONE', #1679, #659 ) ;
#3137=VECTOR ( 'NONE', #3434, 1000.000000000000000 ) ;
#3140=CARTESIAN_POINT ( 'NONE',  ( 1.820000000000000062, 4.653657836759941744E-16, -3.799999999999999378 ) ) ;
#3152=CARTESIAN_POINT ( 'NONE',  ( 1.300000000000000044, 0.7216878364870328300, 1.249999999999999778 ) ) ;
#3156=VERTEX_POINT ( 'NONE', #2110 ) ;
#3162=ORIENTED_EDGE ( 'NONE', *, *, #1205, .T. ) ;
#3164=ORIENTED_EDGE ( 'NONE', *, *, #3006, .T. ) ;
#3168=DIRECTION ( 'NONE',  ( 0.000000000000000000, 0.000000000000000000, 1.000000000000000000 ) ) ;
#3170=APPLICATION_CONTEXT ( 'automotive_design' ) ;
#3173=ORIENTED_EDGE ( 'NONE', *, *, #2747, .F. ) ;
#3181=VERTEX_POINT ( 'NONE', #1177 ) ;
#3183=DIRECTION ( 'NONE',  ( -1.000000000000000000, -0.000000000000000000, -0.000000000000000000 ) ) ;
#3184=AXIS2_PLACEMENT_3D ( 'NONE', #3506, #2541, #2610 ) ;
#3186=EDGE_CURVE ( 'NONE', #1392, #818, #3317, .T. ) ;
#3189=FACE_OUTER_BOUND ( 'NONE', #986, .T. ) ;
#3194=DIRECTION ( 'NONE',  ( 1.000000000000000000, 0.000000000000000000, 0.000000000000000000 ) ) ;
#3195=ADVANCED_FACE ( 'NONE', ( #51 ), #1237, .T. ) ;
#3198=PLANE ( 'NONE',  #3184 ) ;
#3211=DIRECTION ( 'NONE',  ( 0.000000000000000000, 0.000000000000000000, 1.000000000000000000 ) ) ;
#3215=FACE_OUTER_BOUND ( 'NONE', #3474, .T. ) ;
#3219=ORIENTED_EDGE ( 'NONE', *, *, #2447, .T. ) ;
#3220=CARTESIAN_POINT ( 'NONE',  ( 10.20000000000000107, 0.000000000000000000, 0.000000000000000000 ) ) ;
#3227=DIRECTION ( 'NONE',  ( 0.000000000000000000, 0.000000000000000000, 1.000000000000000000 ) ) ;
#3233=ORIENTED_EDGE ( 'NONE', *, *, #1251, .F. ) ;
#3243=CARTESIAN_POINT ( 'NONE',  ( 2.400000000000000799, 0.000000000000000000, 0.000000000000000000 ) ) ;
#3247=EDGE_LOOP ( 'NONE', ( #2016, #2987, #628 ) ) ;
#3249=LINE ( 'NONE', #1189, #18 ) ;
#3251=AXIS2_PLACEMENT_3D ( 'NONE', #1034, #3404, #1921 ) ;
#3252=CIRCLE ( 'NONE', #584, 1.999999999999999112 ) ;
#3253=MANIFOLD_SOLID_BREP ( 'Hex', #1541 ) ;
#3258=EDGE_LOOP ( 'NONE', ( #585, #2410, #2749, #1224 ) ) ;
#3261=AXIS2_PLACEMENT_3D ( 'NONE', #488, #3482, #526 ) ;
#3262=CIRCLE ( 'NONE', #2281, 1.249999999999999778 ) ;
#3277=VERTEX_POINT ( 'NONE', #136 ) ;
#3280=ORIENTED_EDGE ( 'NONE', *, *, #2434, .F. ) ;
#3284=DIRECTION ( 'NONE',  ( 1.000000000000000000, 0.000000000000000000, 0.000000000000000000 ) ) ;
#3287=ORIENTED_EDGE ( 'NONE', *, *, #2358, .T. ) ;
#3294=DIRECTION ( 'NONE',  ( -1.000000000000000000, 0.000000000000000000, 0.000000000000000000 ) ) ;
#3298=ORIENTED_EDGE ( 'NONE', *, *, #3186, .F. ) ;
#3299=DIRECTION ( 'NONE',  ( 0.000000000000000000, 0.000000000000000000, 1.000000000000000000 ) ) ;
#3300=CARTESIAN_POINT ( 'NONE',  ( 2.200000000000000622, 1.999999999999999112, 0.000000000000000000 ) ) ;
#3309=CIRCLE ( 'NONE', #1631, 3.799999999999999378 ) ;
#3310=AXIS2_PLACEMENT_3D ( 'NONE', #2779, #105, #1300 ) ;
#3311=LINE ( 'NONE', #3046, #3088 ) ;
#3315=AXIS2_PLACEMENT_3D ( 'NONE', #2543, #1915, #2460 ) ;
#3317=LINE ( 'NONE', #2660, #1210 ) ;
#3323=CARTESIAN_POINT ( 'NONE',  ( 1.300000000000000044, -0.7216878364870319418, 1.249999999999999778 ) ) ;
#3330=DIRECTION ( 'NONE',  ( 0.000000000000000000, 0.8660254037844387076, 0.4999999999999998890 ) ) ;
#3333=AXIS2_PLACEMENT_3D ( 'NONE', #2143, #3062, #2179 ) ;
#3335=CARTESIAN_POINT ( 'NONE',  ( 3.885274725274726393, -8.673617379884035472E-16, 0.000000000000000000 ) ) ;
#3356=DIRECTION ( 'NONE',  ( -0.000000000000000000, -0.4999999999999999445, -0.8660254037844387076 ) ) ;
#3358=FACE_OUTER_BOUND ( 'NONE', #2971, .T. ) ;
#3361=DIRECTION ( 'NONE',  ( -0.7071067811865492381, 0.000000000000000000, 0.7071067811865457964 ) ) ;
#3368=CARTESIAN_POINT ( 'NONE',  ( 1.300000000000000044, 0.000000000000000000, 1.249999999999999778 ) ) ;
#3370=ADVANCED_FACE ( 'NONE', ( #1391 ), #3198, .T. ) ;
#3372=CIRCLE ( 'NONE', #442, 3.799999999999999378 ) ;
#3383=DIRECTION ( 'NONE',  ( -1.000000000000000000, -0.000000000000000000, -0.000000000000000000 ) ) ;
#3384=AXIS2_PLACEMENT_3D ( 'NONE', #3547, #2384, #650 ) ;
#3385=CARTESIAN_POINT ( 'NONE',  ( 10.20000000000000107, 0.000000000000000000, 1.610000000000000098 ) ) ;
#3396=CARTESIAN_POINT ( 'NONE',  ( 0.000000000000000000, 0.000000000000000000, 0.000000000000000000 ) ) ;
#3397=PRODUCT ( 'socket button head screw_iso_ISO 7380 - M4 x 8 - 8N', 'socket button head screw_iso_ISO 7380 - M4 x 8 - 8N', '', ( #1061 ) ) ;
#3404=DIRECTION ( 'NONE',  ( -1.000000000000000000, -0.000000000000000000, -0.000000000000000000 ) ) ;
#3408=( NAMED_UNIT ( * ) PLANE_ANGLE_UNIT ( ) SI_UNIT ( $, .RADIAN. ) );
#3422=ORIENTED_EDGE ( 'NONE', *, *, #2216, .T. ) ;
#3425=PRESENTATION_STYLE_ASSIGNMENT (( #125 ) ) ;
#3433=EDGE_LOOP ( 'NONE', ( #1930, #2220 ) ) ;
#3434=DIRECTION ( 'NONE',  ( -1.000000000000000000, 0.000000000000000000, 0.000000000000000000 ) ) ;
#3436=CARTESIAN_POINT ( 'NONE',  ( 1.300000000000000044, 1.443375672974065216, 7.017607234860990640E-28 ) ) ;
#3440=DIRECTION ( 'NONE',  ( -0.000000000000000000, 0.5000000000000001110, 0.8660254037844385966 ) ) ;
#3445=EDGE_LOOP ( 'NONE', ( #1857, #1084, #1001, #3682, #799, #548 ) ) ;
#3451=DIRECTION ( 'NONE',  ( 0.000000000000000000, 0.000000000000000000, 1.000000000000000000 ) ) ;
#3458=CARTESIAN_POINT ( 'NONE',  ( 8.673617379884035472E-16, 1.899999999999999689, 0.000000000000000000 ) ) ;
#3462=DIRECTION ( 'NONE',  ( 0.000000000000000000, 0.000000000000000000, -1.000000000000000000 ) ) ;
#3474=EDGE_LOOP ( 'NONE', ( #1439, #2797 ) ) ;
#3476=DIRECTION ( 'NONE',  ( -0.000000000000000000, 0.5000000000000001110, 0.8660254037844385966 ) ) ;
#3481=CARTESIAN_POINT ( 'NONE',  ( 1.300000000000000044, -0.7216878364870318308, -1.250000000000000000 ) ) ;
#3482=DIRECTION ( 'NONE',  ( -1.000000000000000000, -0.000000000000000000, -0.000000000000000000 ) ) ;
#3486=EDGE_CURVE ( 'NONE', #1784, #2381, #3309, .T. ) ;
#3488=DIRECTION ( 'NONE',  ( 0.000000000000000000, 0.000000000000000000, 1.000000000000000000 ) ) ;
#3490=DIRECTION ( 'NONE',  ( -0.000000000000000000, -1.000000000000000000, -0.000000000000000000 ) ) ;
#3500=VECTOR ( 'NONE', #3476, 1000.000000000000000 ) ;
#3504=LINE ( 'NONE', #3481, #1257 ) ;
#3506=CARTESIAN_POINT ( 'NONE',  ( 1.300000000000000044, 0.7216878364870328300, 1.249999999999999778 ) ) ;
#3510=VERTEX_POINT ( 'NONE', #2946 ) ;
#3512=ORIENTED_EDGE ( 'NONE', *, *, #825, .T. ) ;
#3514=EDGE_CURVE ( 'NONE', #3016, #2228, #271, .T. ) ;
#3521=DIRECTION ( 'NONE',  ( 0.000000000000000000, 0.000000000000000000, 1.000000000000000000 ) ) ;
#3523=ORIENTED_EDGE ( 'NONE', *, *, #3045, .T. ) ;
#3530=ORIENTED_EDGE ( 'NONE', *, *, #2358, .F. ) ;
#3533=CARTESIAN_POINT ( 'NONE',  ( 2.200000000000000178, 4.653657836759941744E-16, -3.799999999999999378 ) ) ;
#3536=DIRECTION ( 'NONE',  ( 0.000000000000000000, 0.000000000000000000, 1.000000000000000000 ) ) ;
#3539=ORIENTED_EDGE ( 'NONE', *, *, #1540, .T. ) ;
#3543=CARTESIAN_POINT ( 'NONE',  ( 1.300000000000000044, 0.7216878364870328300, 1.249999999999999778 ) ) ;
#3546=EDGE_LOOP ( 'NONE', ( #2811, #2391, #1546 ) ) ;
#3547=CARTESIAN_POINT ( 'NONE',  ( 1.300000000000000044, -0.7216878364870319418, 1.249999999999999778 ) ) ;
#3552=FACE_OUTER_BOUND ( 'NONE', #2740, .T. ) ;
#3559=VERTEX_POINT ( 'NONE', #1779 ) ;
#3561=DIRECTION ( 'NONE',  ( -0.000000000000000000, 0.4999999999999998890, -0.8660254037844387076 ) ) ;
#3564=EDGE_CURVE ( 'NONE', #2217, #1478, #1494, .T. ) ;
#3565=EDGE_CURVE ( 'NONE', #3065, #698, #325, .T. ) ;
#3570=CIRCLE ( 'NONE', #451, 0.2000000000000000944 ) ;
#3574=LINE ( 'NONE', #2681, #1828 ) ;
#3579=ORIENTED_EDGE ( 'NONE', *, *, #2064, .T. ) ;
#3580=DIRECTION ( 'NONE',  ( -0.000000000000000000, 1.000000000000000000, -0.000000000000000000 ) ) ;
#3584=EDGE_LOOP ( 'NONE', ( #3233, #3579, #1890, #2651 ) ) ;
#3587=CARTESIAN_POINT ( 'NONE',  ( 4.336808689942017736E-16, 0.000000000000000000, 0.000000000000000000 ) ) ;
#3595=ORIENTED_EDGE ( 'NONE', *, *, #3045, .F. ) ;
#3607=ORIENTED_EDGE ( 'NONE', *, *, #825, .F. ) ;
#3617=FACE_OUTER_BOUND ( 'NONE', #1645, .T. ) ;
#3618=CARTESIAN_POINT ( 'NONE',  ( 1.300000000000000044, 0.7216878364870328300, -1.250000000000000000 ) ) ;
#3620=AXIS2_PLACEMENT_3D ( 'NONE', #2362, #565, #2305 ) ;
#3626=CARTESIAN_POINT ( 'NONE',  ( 1.300000000000000044, -1.443375672974063884, -3.691112476943992763E-18 ) ) ;
#3629=VERTEX_POINT ( 'NONE', #3368 ) ;
#3633=DIRECTION ( 'NONE',  ( 0.000000000000000000, 0.000000000000000000, 1.000000000000000000 ) ) ;
#3634=CARTESIAN_POINT ( 'NONE',  ( 0.000000000000000000, 1.443375672974065216, 7.017607234860990640E-28 ) ) ;
#3652=DIRECTION ( 'NONE',  ( 0.000000000000000000, 0.000000000000000000, -1.000000000000000000 ) ) ;
#3659=DIRECTION ( 'NONE',  ( 0.000000000000000000, 0.4999999999999999445, 0.8660254037844387076 ) ) ;
#3665=LINE ( 'NONE', #1280, #708 ) ;
#3671=ORIENTED_EDGE ( 'NONE', *, *, #1000, .F. ) ;
#3677=AXIS2_PLACEMENT_3D ( 'NONE', #1456, #1492, #1211 ) ;
#3679=EDGE_CURVE ( 'NONE', #3156, #535, #983, .T. ) ;
#3682=ORIENTED_EDGE ( 'NONE', *, *, #3565, .T. ) ;
#3686=CIRCLE ( 'NONE', #3251, 1.249999999999999778 ) ;
#3700=EDGE_CURVE ( 'NONE', #2659, #2253, #421, .T. ) ;
#3702=VECTOR ( 'NONE', #2189, 1000.000000000000000 ) ;
#3714=SPHERICAL_SURFACE ( 'NONE', #2582, 4.324969328314201888 ) ;
#3715=DIRECTION ( 'NONE',  ( -1.000000000000000000, -0.000000000000000000, -0.000000000000000000 ) ) ;
#3721=SHAPE_REPRESENTATION_RELATIONSHIP ( 'NONE' , 'NONE' ,  #3744, #1526 ) ;
#3727=FACE_OUTER_BOUND ( 'NONE', #3584, .T. ) ;
#3731=PLANE ( 'NONE',  #903 ) ;
#3742=SHAPE_DEFINITION_REPRESENTATION ( #2803, #3744 ) ;
#3744=SHAPE_REPRESENTATION ( 'socket button head screw_iso_ISO 7380 - M4 x 8 - 8N', ( #2207 ), #2713 ) ;
#3749=DIRECTION ( 'NONE',  ( -1.000000000000000000, 0.000000000000000000, 0.000000000000000000 ) ) ;
#3755=LINE ( 'NONE', #3827, #3500 ) ;
#3756=AXIS2_PLACEMENT_3D ( 'NONE', #2392, #3284, #2100 ) ;
#3760=CIRCLE ( 'NONE', #2635, 1.610000000000000098 ) ;
#3762=CARTESIAN_POINT ( 'NONE',  ( 1.300000000000000044, -1.443375672974063884, -3.691112476943992763E-18 ) ) ;
#3770=ORIENTED_EDGE ( 'NONE', *, *, #3564, .T. ) ;
#3788=CARTESIAN_POINT ( 'NONE',  ( 0.000000000000000000, -0.7216878364870318308, -1.250000000000000000 ) ) ;
#3789=ORIENTED_EDGE ( 'NONE', *, *, #867, .T. ) ;
#3790=CARTESIAN_POINT ( 'NONE',  ( 1.300000000000000044, -0.7216878364870318308, 1.249999999999999778 ) ) ;
#3792=EDGE_LOOP ( 'NONE', ( #3808, #312 ) ) ;
#3803=CARTESIAN_POINT ( 'NONE',  ( 2.400000000000000799, 2.694222958124176020E-16, -2.199999999999999289 ) ) ;
#3808=ORIENTED_EDGE ( 'NONE', *, *, #2922, .T. ) ;
#3813=AXIS2_PLACEMENT_3D ( 'NONE', #1817, #2151, #2976 ) ;
#3822=VERTEX_POINT ( 'NONE', #156 ) ;
#3826=CIRCLE ( 'NONE', #2341, 4.324969328314201888 ) ;
#3827=CARTESIAN_POINT ( 'NONE',  ( 0.000000000000000000, 1.443375672974065216, 7.017607234860990640E-28 ) ) ;
#3829=ADVANCED_FACE ( 'NONE', ( #1117 ), #1350, .T. ) ;
#3838=LINE ( 'NONE', #53, #75 ) ;
#3875=COLOUR_RGB('Black',0.12,0.14,0.17);
#3876=FILL_AREA_STYLE_COLOUR('',#3875);
#3877=FILL_AREA_STYLE('',(#3876));
#3878=SURFACE_STYLE_FILL_AREA(#3877);
#3879=SURFACE_SIDE_STYLE('',(#3878));
#3880=SURFACE_STYLE_USAGE(.BOTH.,#3879);
#3881=PRESENTATION_STYLE_ASSIGNMENT((#3880));
ENDSEC;
END-ISO-10303-21;
